ISO-10303-21;
HEADER;
FILE_DESCRIPTION (('STEP AP214'),
    '1' );
FILE_NAME ('Mirrorsliding track^MAS-180.step',
    '2026-10-27T17:01:19',
    ( '' ),
    ( '' ),
    'SwSTEP 2.0',
    'SolidWorks 2026',
    '' );
FILE_SCHEMA (( 'AUTOMOTIVE_DESIGN' ));
ENDSEC;

DATA;
#40=VECTOR ( 'NONE', #12593, 1000.000000000000000 ) ;
#59=FACE_OUTER_BOUND ( 'NONE', #3908, .T. ) ;
#75=CARTESIAN_POINT ( 'NONE',  ( 609.6905198467529772, 186.4571330906553044, -187.4188186979287423 ) ) ;
#87=ADVANCED_FACE ( 'NONE', ( #9552, #4013, #2686 ), #14052, .T. ) ;
#115=ORIENTED_EDGE ( 'NONE', *, *, #8446, .T. ) ;
#117=ORIENTED_EDGE ( 'NONE', *, *, #9862, .T. ) ;
#156=VECTOR ( 'NONE', #9588, 1000.000000000000000 ) ;
#183=CARTESIAN_POINT ( 'NONE',  ( 610.0421465541240877, 190.7920056415575516, -186.9999999999999432 ) ) ;
#198=DIRECTION ( 'NONE',  ( -1.000000000000000000, 0.000000000000000000, 0.000000000000000000 ) ) ;
#229=LINE ( 'NONE', #12418, #8916 ) ;
#286=LINE ( 'NONE', #5042, #1068 ) ;
#319=DIRECTION ( 'NONE',  ( 0.000000000000000000, 0.000000000000000000, 1.000000000000000000 ) ) ;
#323=CARTESIAN_POINT ( 'NONE',  ( -8.505790995054899994, 376.6597771564184427, -184.8000000000000398 ) ) ;
#342=SHAPE_REPRESENTATION ( 'Mirrorsliding track^MAS-180', ( #9440 ), #8524 ) ;
#345=( NAMED_UNIT ( * ) SI_UNIT ( $, .STERADIAN. ) SOLID_ANGLE_UNIT ( ) );
#357=EDGE_CURVE ( 'NONE', #9335, #3684, #13663, .T. ) ;
#366=CARTESIAN_POINT ( 'NONE',  ( 610.6379424248335681, 188.7103817868187150, -185.3679143846944157 ) ) ;
#368=DIRECTION ( 'NONE',  ( -0.000000000000000000, -0.000000000000000000, 1.000000000000000000 ) ) ;
#373=EDGE_CURVE ( 'NONE', #10071, #11808, #3015, .T. ) ;
#388=CARTESIAN_POINT ( 'NONE',  ( 137.1540310085880776, 355.9707293956415697, -187.0000000000000000 ) ) ;
#400=DIRECTION ( 'NONE',  ( -1.000000000000000000, -0.000000000000000000, -0.000000000000000000 ) ) ;
#404=B_SPLINE_CURVE_WITH_KNOTS ( 'NONE', 3,
 ( #2265, #183, #10248, #7370, #11863, #11785, #14168, #411, #1689, #6194, #9441, #1819, #12981, #9584, #6332, #8391 ),
 .UNSPECIFIED., .F., .F.,
 ( 4, 2, 2, 2, 2, 2, 2, 4 ),
 ( 8.777083671441753062E-17, 0.0009429092714760194203, 0.001414363907214010374, 0.001885818542952001327, 0.002357273178689992064, 0.002828727814427983017, 0.003300182450165973971, 0.003771637085903964924 ),
 .UNSPECIFIED. ) ;
#411=CARTESIAN_POINT ( 'NONE',  ( 610.3331342679523459, 189.2775297294220991, -186.2537089296249349 ) ) ;
#419=CARTESIAN_POINT ( 'NONE',  ( 137.1540310085880776, 355.9707293956415697, -187.0000000000000000 ) ) ;
#507=EDGE_CURVE ( 'NONE', #1236, #9769, #286, .T. ) ;
#519=FACE_OUTER_BOUND ( 'NONE', #5861, .T. ) ;
#540=DIRECTION ( 'NONE',  ( 0.000000000000000000, 1.000000000000000000, 0.000000000000000000 ) ) ;
#583=EDGE_CURVE ( 'NONE', #4552, #13350, #10638, .T. ) ;
#590=ADVANCED_FACE ( 'NONE', ( #11807 ), #6209, .F. ) ;
#642=DIRECTION ( 'NONE',  ( 0.2873478855663454401, 0.9578262852211514300, 3.831370512995697396E-15 ) ) ;
#645=DIRECTION ( 'NONE',  ( 0.9578262852211513190, -0.2873478855663454401, -1.972152263052529951E-31 ) ) ;
#661=CARTESIAN_POINT ( 'NONE',  ( 609.9641659369621038, 190.7604956903689413, -190.0000000000000568 ) ) ;
#662=VECTOR ( 'NONE', #3204, 1000.000000000000114 ) ;
#667=DIRECTION ( 'NONE',  ( 0.000000000000000000, -0.000000000000000000, 1.000000000000000000 ) ) ;
#676=AXIS2_PLACEMENT_3D ( 'NONE', #13441, #1099, #7762 ) ;
#678=LINE ( 'NONE', #11970, #4723 ) ;
#694=SURFACE_STYLE_USAGE ( .BOTH. , #13045 ) ;
#700=DIRECTION ( 'NONE',  ( 0.9578262852211514300, -0.2873478855663454401, -0.000000000000000000 ) ) ;
#731=VECTOR ( 'NONE', #4764, 1000.000000000000000 ) ;
#746=CARTESIAN_POINT ( 'NONE',  ( 609.8615525982525014, 189.7413297629623514, -189.8335177487570888 ) ) ;
#762=EDGE_LOOP ( 'NONE', ( #6323, #4828, #8477, #7125 ) ) ;
#767=CARTESIAN_POINT ( 'NONE',  ( -10.00000000000002487, 371.6790804732684705, -184.8000000000000114 ) ) ;
#788=ORIENTED_EDGE ( 'NONE', *, *, #7769, .F. ) ;
#801=DIRECTION ( 'NONE',  ( 0.9578262852211514300, -0.2873478855663453846, 1.407442229263725984E-15 ) ) ;
#811=PLANE ( 'NONE',  #6832 ) ;
#814=AXIS2_PLACEMENT_3D ( 'NONE', #10708, #801, #10929 ) ;
#829=EDGE_CURVE ( 'NONE', #12655, #11808, #12315, .T. ) ;
#861=DIRECTION ( 'NONE',  ( -0.9578262852211513190, 0.2873478855663453846, 0.000000000000000000 ) ) ;
#887=ORIENTED_EDGE ( 'NONE', *, *, #14587, .T. ) ;
#962=PRODUCT_DEFINITION_SHAPE ( 'NONE', 'NONE',  #8642 ) ;
#986=CARTESIAN_POINT ( 'NONE',  ( 609.9277849535120595, 190.4148309465319358, -190.0300000000000296 ) ) ;
#1033=CARTESIAN_POINT ( 'NONE',  ( 610.0000000000000000, 227.4403065089105951, -187.0000000000000000 ) ) ;
#1046=EDGE_CURVE ( 'NONE', #3037, #4895, #2875, .T. ) ;
#1053=CARTESIAN_POINT ( 'NONE',  ( 609.7412162373094588, 188.4357741873886880, -189.3699028110927429 ) ) ;
#1057=DIRECTION ( 'NONE',  ( -0.2873478855663437193, -0.9578262852211517631, -0.000000000000000000 ) ) ;
#1068=VECTOR ( 'NONE', #5913, 1000.000000000000114 ) ;
#1092=DIRECTION ( 'NONE',  ( -1.000000000000000000, 0.000000000000000000, 0.000000000000000000 ) ) ;
#1099=DIRECTION ( 'NONE',  ( -0.000000000000000000, -0.000000000000000000, 1.000000000000000000 ) ) ;
#1110=DIRECTION ( 'NONE',  ( 0.000000000000000000, 0.000000000000000000, -1.000000000000000000 ) ) ;
#1116=MECHANICAL_DESIGN_GEOMETRIC_PRESENTATION_REPRESENTATION('',(#7730),#6784);
#1122=CARTESIAN_POINT ( 'NONE',  ( 609.8579287883226243, 189.7296425882048823, -189.8646579186752774 ) ) ;
#1170=CARTESIAN_POINT ( 'NONE',  ( 446.3084422793565409, 264.0194060144110608, -190.0000000000000000 ) ) ;
#1206=CARTESIAN_POINT ( 'NONE',  ( 610.0835668916889745, 190.4817695994259736, -186.9427398886703315 ) ) ;
#1213=B_SPLINE_SURFACE_WITH_KNOTS ( 'NONE', 1, 3, ( 
 ( #6681, #986, #9036, #1053, #5504, #11241, #5562, #10061, #7866, #14568 ),
 ( #2300, #4459, #1122, #9178, #5635, #6812, #75, #13540, #3426, #12493 ),
 ( #9102, #13685, #1206, #10218, #3497, #7991, #6893, #8289, #4835, #13761 ),
 ( #12799, #1502, #10658, #7031, #11533, #7115, #13904, #366, #13824, #1643 ) ),
 .UNSPECIFIED., .F., .F., .F.,
 ( 2, 1, 1, 2 ),
 ( 4, 2, 2, 2, 4 ),
 ( -0.01000000000000000021, 0.000000000000000000, 1.000000000000000000, 1.010099999999999998 ),
 ( 0.000000000000000000, 0.2500000000000000000, 0.5000000000000000000, 0.7500000000000000000, 1.000000000000000000 ),
 .UNSPECIFIED. ) ;
#1214=EDGE_CURVE ( 'NONE', #7124, #3179, #229, .T. ) ;
#1218=VERTEX_POINT ( 'NONE', #11321 ) ;
#1233=LINE ( 'NONE', #1302, #40 ) ;
#1236=VERTEX_POINT ( 'NONE', #9402 ) ;
#1273=EDGE_CURVE ( 'NONE', #12403, #5365, #10729, .T. ) ;
#1301=DIRECTION ( 'NONE',  ( 0.000000000000000000, -1.000000000000000000, 0.000000000000000000 ) ) ;
#1302=CARTESIAN_POINT ( 'NONE',  ( -9.511508594537124495, 378.5275384125996538, -187.0000000000000284 ) ) ;
#1357=ORIENTED_EDGE ( 'NONE', *, *, #9348, .F. ) ;
#1368=CARTESIAN_POINT ( 'NONE',  ( 610.0000000000000000, 227.4403065089105951, -190.0000000000000000 ) ) ;
#1410=CARTESIAN_POINT ( 'NONE',  ( -8.505790995054894665, 376.6597771564184427, -184.8000000000000398 ) ) ;
#1420=CARTESIAN_POINT ( 'NONE',  ( 610.0000000000002274, 185.6790804732676747, 8.443403382996446544E-13 ) ) ;
#1456=VERTEX_POINT ( 'NONE', #9912 ) ;
#1498=LINE ( 'NONE', #10496, #8925 ) ;
#1502=CARTESIAN_POINT ( 'NONE',  ( 610.0429133068968213, 190.7986032820865319, -186.9697000000000173 ) ) ;
#1541=EDGE_LOOP ( 'NONE', ( #3116, #12222, #10523, #7416 ) ) ;
#1576=EDGE_CURVE ( 'NONE', #4895, #4552, #10097, .T. ) ;
#1642=DIRECTION ( 'NONE',  ( -1.000000000000000000, 0.000000000000000000, 0.000000000000000000 ) ) ;
#1643=CARTESIAN_POINT ( 'NONE',  ( 610.8707502976318438, 188.5815814653741427, -184.8000000000000682 ) ) ;
#1678=ORIENTED_EDGE ( 'NONE', *, *, #9942, .T. ) ;
#1689=CARTESIAN_POINT ( 'NONE',  ( 610.3687250539534261, 189.1718658564638247, -186.1427899493634470 ) ) ;
#1694=LINE ( 'NONE', #5094, #156 ) ;
#1695=EDGE_LOOP ( 'NONE', ( #14289, #6398, #3405, #4458 ) ) ;
#1714=DIRECTION ( 'NONE',  ( -0.2873478855663453291, -0.9578262852211513190, -3.835990623682899812E-15 ) ) ;
#1719=CARTESIAN_POINT ( 'NONE',  ( 609.9288325809317257, 190.4177448864037956, -189.9663414180174925 ) ) ;
#1782=ADVANCED_FACE ( 'NONE', ( #519 ), #7170, .T. ) ;
#1819=CARTESIAN_POINT ( 'NONE',  ( 610.5828669213532294, 188.7537838752662935, -185.5093481647506906 ) ) ;
#1828=CARTESIAN_POINT ( 'NONE',  ( 610.8620436566991430, 188.5525593289318351, -169.9999999999999716 ) ) ;
#1839=CIRCLE ( 'NONE', #5617, 2.649999999999985700 ) ;
#1866=VECTOR ( 'NONE', #645, 1000.000000000000227 ) ;
#1868=ORIENTED_EDGE ( 'NONE', *, *, #11880, .F. ) ;
#1892=ORIENTED_EDGE ( 'NONE', *, *, #3203, .F. ) ;
#1926=CARTESIAN_POINT ( 'NONE',  ( 610.0000000000001137, 185.6790804732684421, -184.8000000000000682 ) ) ;
#1962=( NAMED_UNIT ( * ) PLANE_ANGLE_UNIT ( ) SI_UNIT ( $, .RADIAN. ) );
#1967=DIRECTION ( 'NONE',  ( 0.9578262852211489875, -0.2873478855663534892, 0.000000000000000000 ) ) ;
#2011=FACE_OUTER_BOUND ( 'NONE', #10735, .T. ) ;
#2060=FACE_OUTER_BOUND ( 'NONE', #6298, .T. ) ;
#2075=VERTEX_POINT ( 'NONE', #9006 ) ;
#2138=EDGE_LOOP ( 'NONE', ( #117, #4853, #8394, #887 ) ) ;
#2214=EDGE_CURVE ( 'NONE', #1456, #4552, #1694, .T. ) ;
#2219=DIRECTION ( 'NONE',  ( 0.9578262852211513190, -0.2873478855663453291, 0.000000000000000000 ) ) ;
#2234=DIRECTION ( 'NONE',  ( 0.000000000000000000, 1.000000000000000000, 0.000000000000000000 ) ) ;
#2265=CARTESIAN_POINT ( 'NONE',  ( 610.0000000000001137, 191.1080398579018720, -187.0000000000000000 ) ) ;
#2300=CARTESIAN_POINT ( 'NONE',  ( 610.0000000000001137, 191.1080398579019288, -190.0000000000000284 ) ) ;
#2308=EDGE_LOOP ( 'NONE', ( #3923, #3714, #6296, #3982 ) ) ;
#2318=DIRECTION ( 'NONE',  ( -0.2873478855663446629, -0.9578262852211516520, -5.337610695313252962E-15 ) ) ;
#2486=ORIENTED_EDGE ( 'NONE', *, *, #7998, .T. ) ;
#2497=ORIENTED_EDGE ( 'NONE', *, *, #9135, .F. ) ;
#2507=CARTESIAN_POINT ( 'NONE',  ( 446.3084422793565409, 264.0194060144110608, -187.0000000000000000 ) ) ;
#2509=DIRECTION ( 'NONE',  ( 0.9578262852211514300, -0.2873478855663454401, -0.000000000000000000 ) ) ;
#2510=DIRECTION ( 'NONE',  ( 0.000000000000000000, 0.000000000000000000, -1.000000000000000000 ) ) ;
#2516=PLANE ( 'NONE',  #6764 ) ;
#2535=LINE ( 'NONE', #11680, #11313 ) ;
#2545=DIRECTION ( 'NONE',  ( -1.000000000000000000, 0.000000000000000000, 0.000000000000000000 ) ) ;
#2548=AXIS2_PLACEMENT_3D ( 'NONE', #9623, #14273, #4103 ) ;
#2584=ADVANCED_FACE ( 'NONE', ( #6509 ), #11218, .F. ) ;
#2587=MANIFOLD_SOLID_BREP ( '<sliding track>-<M5 Clearance Hole1>', #13758 ) ;
#2593=VERTEX_POINT ( 'NONE', #9305 ) ;
#2595=EDGE_CURVE ( 'NONE', #5365, #6317, #8435, .T. ) ;
#2608=VECTOR ( 'NONE', #1714, 1000.000000000000227 ) ;
#2632=VECTOR ( 'NONE', #7245, 1000.000000000000000 ) ;
#2652=CARTESIAN_POINT ( 'NONE',  ( -9.999999999999957367, 376.8992337277236970, -190.0000000000000000 ) ) ;
#2673=CARTESIAN_POINT ( 'NONE',  ( 610.8620436566991430, 188.5525593289319488, -184.8000000000000398 ) ) ;
#2686=FACE_OUTER_BOUND ( 'NONE', #8957, .T. ) ;
#2729=ADVANCED_FACE ( 'NONE', ( #2883 ), #5033, .T. ) ;
#2733=CARTESIAN_POINT ( 'NONE',  ( -9.999999999999998224, 376.8992337277234128, -187.0000000000000000 ) ) ;
#2738=ORIENTED_EDGE ( 'NONE', *, *, #507, .T. ) ;
#2748=EDGE_CURVE ( 'NONE', #3179, #9848, #7299, .T. ) ;
#2794=ORIENTED_EDGE ( 'NONE', *, *, #357, .T. ) ;
#2813=CIRCLE ( 'NONE', #5647, 2.199999999999984635 ) ;
#2875=LINE ( 'NONE', #6744, #12921 ) ;
#2883=FACE_OUTER_BOUND ( 'NONE', #2138, .T. ) ;
#2906=CARTESIAN_POINT ( 'NONE',  ( -10.00000000000045297, 371.6790804732678453, 1.178702027242996938E-12 ) ) ;
#2930=DIRECTION ( 'NONE',  ( 0.000000000000000000, 0.000000000000000000, -1.000000000000000000 ) ) ;
#2962=LINE ( 'NONE', #4218, #14159 ) ;
#2969=CARTESIAN_POINT ( 'NONE',  ( 609.7493509738548028, 188.4639666770506494, -189.3135794259398494 ) ) ;
#2985=LINE ( 'NONE', #9991, #9709 ) ;
#2997=CARTESIAN_POINT ( 'NONE',  ( -9.511508594537124495, 378.5275384125996538, -187.0000000000000284 ) ) ;
#3012=CARTESIAN_POINT ( 'NONE',  ( -8.074769166705396017, 378.0965165842501392, -187.0000000000000284 ) ) ;
#3015=CIRCLE ( 'NONE', #11480, 2.649999999999985700 ) ;
#3037=VERTEX_POINT ( 'NONE', #3835 ) ;
#3042=CARTESIAN_POINT ( 'NONE',  ( 609.8848581100098727, 185.7487647174620520, -185.4822770966949008 ) ) ;
#3112=LINE ( 'NONE', #9681, #6582 ) ;
#3116=ORIENTED_EDGE ( 'NONE', *, *, #8157, .T. ) ;
#3121=CARTESIAN_POINT ( 'NONE',  ( 609.7152679600854981, 186.3148376777868975, -187.1062553063055418 ) ) ;
#3124=DIRECTION ( 'NONE',  ( -2.449021377849607626E-15, -3.265361837132810036E-15, 1.000000000000000000 ) ) ;
#3129=ADVANCED_FACE ( 'NONE', ( #2011 ), #10526, .F. ) ;
#3176=CARTESIAN_POINT ( 'NONE',  ( -9.511508594537124495, 378.5275384125996538, -187.0000000000000284 ) ) ;
#3179=VERTEX_POINT ( 'NONE', #5630 ) ;
#3190=B_SPLINE_CURVE_WITH_KNOTS ( 'NONE', 3,
 ( #14112, #661, #1719, #746, #8503, #13085, #2969, #9767, #11890, #10720, #8646, #6363, #5330, #13227, #3121, #7463, #14264, #3042, #6512, #7625 ),
 .UNSPECIFIED., .F., .F.,
 ( 4, 2, 2, 2, 2, 2, 2, 2, 2, 4 ),
 ( 5.551115123125782702E-17, 0.001037574205614438111, 0.002075148411228820711, 0.003112722616843203310, 0.003631509719650373360, 0.004150296822457543409, 0.005187871028071766415, 0.006225445233685987685, 0.007263019439300210690, 0.008300593644914432828 ),
 .UNSPECIFIED. ) ;
#3199=DIRECTION ( 'NONE',  ( 0.2873478855663437748, 0.9578262852211518741, 0.000000000000000000 ) ) ;
#3203=EDGE_CURVE ( 'NONE', #12661, #9848, #9030, .T. ) ;
#3204=DIRECTION ( 'NONE',  ( 0.2873478855663452736, 0.9578262852211513190, 3.491481338843133355E-15 ) ) ;
#3227=PLANE ( 'NONE',  #6191 ) ;
#3314=AXIS2_PLACEMENT_3D ( 'NONE', #12388, #5690, #10192 ) ;
#3325=ORIENTED_EDGE ( 'NONE', *, *, #3339, .T. ) ;
#3339=EDGE_CURVE ( 'NONE', #4895, #2075, #1498, .T. ) ;
#3342=CIRCLE ( 'NONE', #11349, 2.649999999999985700 ) ;
#3346=CARTESIAN_POINT ( 'NONE',  ( 610.0000000000000000, 227.4403065089105951, -187.0000000000000000 ) ) ;
#3361=ORIENTED_EDGE ( 'NONE', *, *, #3492, .T. ) ;
#3362=FACE_OUTER_BOUND ( 'NONE', #1541, .T. ) ;
#3370=ORIENTED_EDGE ( 'NONE', *, *, #7769, .T. ) ;
#3383=AXIS2_PLACEMENT_3D ( 'NONE', #3722, #667, #1642 ) ;
#3399=CARTESIAN_POINT ( 'NONE',  ( 448.9584422793565750, 264.0194060144110608, -187.0000000000000000 ) ) ;
#3405=ORIENTED_EDGE ( 'NONE', *, *, #1576, .F. ) ;
#3426=CARTESIAN_POINT ( 'NONE',  ( 609.8754609228352592, 185.7164421964179439, -185.4807968138250374 ) ) ;
#3431=DIRECTION ( 'NONE',  ( -1.000000000000000000, 0.000000000000000000, 0.000000000000000000 ) ) ;
#3434=DIRECTION ( 'NONE',  ( -1.000000000000000000, 0.000000000000000000, 0.000000000000000000 ) ) ;
#3492=EDGE_CURVE ( 'NONE', #13350, #2075, #3190, .T. ) ;
#3497=CARTESIAN_POINT ( 'NONE',  ( 610.2340919441475080, 189.6262799281293212, -186.5592670532760167 ) ) ;
#3503=AXIS2_PLACEMENT_3D ( 'NONE', #11873, #642, #14030 ) ;
#3510=EDGE_CURVE ( 'NONE', #4895, #7124, #12931, .T. ) ;
#3533=DIRECTION ( 'NONE',  ( 0.000000000000000000, -1.000000000000000000, 0.000000000000000000 ) ) ;
#3574=VECTOR ( 'NONE', #12685, 1000.000000000000000 ) ;
#3581=AXIS2_PLACEMENT_3D ( 'NONE', #10518, #12883, #6018 ) ;
#3585=ADVANCED_FACE ( 'NONE', ( #59 ), #8936, .F. ) ;
#3600=DIRECTION ( 'NONE',  ( -0.9578262852211514300, 0.2873478855663454401, 0.000000000000000000 ) ) ;
#3633=CARTESIAN_POINT ( 'NONE',  ( 610.0000000000000000, 227.4403065089105951, -190.0000000000000000 ) ) ;
#3684=VERTEX_POINT ( 'NONE', #1033 ) ;
#3690=ORIENTED_EDGE ( 'NONE', *, *, #11875, .T. ) ;
#3714=ORIENTED_EDGE ( 'NONE', *, *, #829, .T. ) ;
#3722=CARTESIAN_POINT ( 'NONE',  ( 0.000000000000000000, 0.000000000000000000, -187.0000000000000000 ) ) ;
#3748=ORIENTED_EDGE ( 'NONE', *, *, #3872, .F. ) ;
#3773=EDGE_LOOP ( 'NONE', ( #5069, #6788, #4171, #788 ) ) ;
#3824=ORIENTED_EDGE ( 'NONE', *, *, #14325, .F. ) ;
#3835=CARTESIAN_POINT ( 'NONE',  ( -9.137956343300853490, 374.5525593289319204, -184.8000000000000398 ) ) ;
#3867=ORIENTED_EDGE ( 'NONE', *, *, #9171, .F. ) ;
#3872=EDGE_CURVE ( 'NONE', #7124, #12661, #14031, .T. ) ;
#3880=CARTESIAN_POINT ( 'NONE',  ( 142.4540310085880606, 355.9707293956415697, -187.0000000000000000 ) ) ;
#3895=PLANE ( 'NONE',  #10767 ) ;
#3902=EDGE_CURVE ( 'NONE', #2593, #7285, #14096, .T. ) ;
#3908=EDGE_LOOP ( 'NONE', ( #9919, #6980, #10427, #10740 ) ) ;
#3923=ORIENTED_EDGE ( 'NONE', *, *, #7567, .T. ) ;
#3937=DIRECTION ( 'NONE',  ( 0.000000000000000000, 0.000000000000000000, -1.000000000000000000 ) ) ;
#3956=CARTESIAN_POINT ( 'NONE',  ( -8.074769166705394241, 378.0965165842501392, -187.0000000000000000 ) ) ;
#3982=ORIENTED_EDGE ( 'NONE', *, *, #11875, .F. ) ;
#4001=ORIENTED_EDGE ( 'NONE', *, *, #12847, .T. ) ;
#4013=FACE_BOUND ( 'NONE', #14383, .T. ) ;
#4041=ORIENTED_EDGE ( 'NONE', *, *, #13021, .F. ) ;
#4055=EDGE_LOOP ( 'NONE', ( #7175, #3824, #2794, #10685 ) ) ;
#4103=DIRECTION ( 'NONE',  ( -0.2873478855663452736, -0.9578262852211514300, 0.000000000000000000 ) ) ;
#4124=ORIENTED_EDGE ( 'NONE', *, *, #829, .F. ) ;
#4139=DIRECTION ( 'NONE',  ( 0.2873478855663454401, 0.9578262852211514300, 3.831370512995697396E-15 ) ) ;
#4148=EDGE_CURVE ( 'NONE', #7897, #13350, #8098, .T. ) ;
#4171=ORIENTED_EDGE ( 'NONE', *, *, #12076, .T. ) ;
#4173=LINE ( 'NONE', #6394, #12732 ) ;
#4207=EDGE_CURVE ( 'NONE', #3684, #7897, #12754, .T. ) ;
#4218=CARTESIAN_POINT ( 'NONE',  ( 103.3965373855728558, 344.6551246185656510, -190.0000000000000000 ) ) ;
#4227=ORIENTED_EDGE ( 'NONE', *, *, #14325, .T. ) ;
#4254=FILL_AREA_STYLE_COLOUR ( '', #8762 ) ;
#4297=EDGE_LOOP ( 'NONE', ( #4001, #7640, #2738, #7734, #9118, #3370, #4712 ) ) ;
#4303=CARTESIAN_POINT ( 'NONE',  ( 610.8620436566991430, 188.5525593289318351, -169.9999999999999716 ) ) ;
#4331=SHAPE_REPRESENTATION_RELATIONSHIP ( 'NONE' , 'NONE' ,  #342, #8625 ) ;
#4339=FACE_OUTER_BOUND ( 'NONE', #7857, .T. ) ;
#4347=CARTESIAN_POINT ( 'NONE',  ( 0.000000000000000000, 0.000000000000000000, 0.000000000000000000 ) ) ;
#4443=EDGE_LOOP ( 'NONE', ( #11982, #9286, #115, #6846 ) ) ;
#4458=ORIENTED_EDGE ( 'NONE', *, *, #1046, .F. ) ;
#4459=CARTESIAN_POINT ( 'NONE',  ( 609.9289135522120660, 190.4185930515760958, -190.0000000000000284 ) ) ;
#4533=ADVANCED_FACE ( 'NONE', ( #4339 ), #5442, .T. ) ;
#4552=VERTEX_POINT ( 'NONE', #13551 ) ;
#4555=FACE_BOUND ( 'NONE', #11560, .T. ) ;
#4589=FACE_OUTER_BOUND ( 'NONE', #1695, .T. ) ;
#4700=FACE_BOUND ( 'NONE', #13236, .T. ) ;
#4712=ORIENTED_EDGE ( 'NONE', *, *, #8221, .T. ) ;
#4723=VECTOR ( 'NONE', #3199, 1000.000000000000114 ) ;
#4764=DIRECTION ( 'NONE',  ( 2.022127743178574844E-16, 3.939404418192334771E-15, -1.000000000000000000 ) ) ;
#4767=MECHANICAL_DESIGN_GEOMETRIC_PRESENTATION_REPRESENTATION('',(#6170),#7109);
#4782=CARTESIAN_POINT ( 'NONE',  ( 0.000000000000000000, 0.000000000000000000, -190.0000000000000000 ) ) ;
#4828=ORIENTED_EDGE ( 'NONE', *, *, #3510, .T. ) ;
#4835=CARTESIAN_POINT ( 'NONE',  ( 610.7375075899259400, 188.5899201489639267, -185.0880224589102454 ) ) ;
#4853=ORIENTED_EDGE ( 'NONE', *, *, #2748, .T. ) ;
#4895=VERTEX_POINT ( 'NONE', #767 ) ;
#4972=VECTOR ( 'NONE', #10473, 1000.000000000000114 ) ;
#4976=CARTESIAN_POINT ( 'NONE',  ( -10.00000000000000000, 413.4403065089105667, -187.0000000000000000 ) ) ;
#5033=PLANE ( 'NONE',  #3503 ) ;
#5042=CARTESIAN_POINT ( 'NONE',  ( 610.0000000000000000, 227.4403065089105951, -190.0000000000000000 ) ) ;
#5045=DIRECTION ( 'NONE',  ( 0.2873478855663470499, 0.9578262852211508749, 0.000000000000000000 ) ) ;
#5061=ADVANCED_FACE ( 'NONE', ( #12916 ), #10985, .F. ) ;
#5069=ORIENTED_EDGE ( 'NONE', *, *, #2214, .F. ) ;
#5094=CARTESIAN_POINT ( 'NONE',  ( -8.505790995054914205, 376.6597771564183859, -187.0000000000000284 ) ) ;
#5112=LINE ( 'NONE', #1420, #2632 ) ;
#5222=( LENGTH_UNIT ( ) NAMED_UNIT ( * ) SI_UNIT ( .MILLI., .METRE. ) );
#5241=CARTESIAN_POINT ( 'NONE',  ( 448.9584422793565750, 264.0194060144110608, -187.0000000000000000 ) ) ;
#5255=PRODUCT_DEFINITION_FORMATION_WITH_SPECIFIED_SOURCE ( 'ANY', '', #7374, .NOT_KNOWN. ) ;
#5318=DIRECTION ( 'NONE',  ( 0.9578262852211489875, -0.2873478855663534892, 0.000000000000000000 ) ) ;
#5330=CARTESIAN_POINT ( 'NONE',  ( 609.6834941627989792, 186.8890602495695248, -187.9755619318007405 ) ) ;
#5354=CARTESIAN_POINT ( 'NONE',  ( -8.074769166705396017, 378.0965165842501392, -187.0000000000000284 ) ) ;
#5365=VERTEX_POINT ( 'NONE', #5968 ) ;
#5421=DIRECTION ( 'NONE',  ( 0.000000000000000000, 0.000000000000000000, -1.000000000000000000 ) ) ;
#5425=VECTOR ( 'NONE', #3533, 1000.000000000000000 ) ;
#5442=CYLINDRICAL_SURFACE ( 'NONE', #12489, 5.199999999999999289 ) ;
#5475=EDGE_LOOP ( 'NONE', ( #4124, #6166, #3690, #2497 ) ) ;
#5490=CARTESIAN_POINT ( 'NONE',  ( 610.0000000000002274, 185.6790804732683284, -169.9999999999999716 ) ) ;
#5491=CARTESIAN_POINT ( 'NONE',  ( 610.0000000000001137, 191.1080398579018720, -187.0000000000000000 ) ) ;
#5504=CARTESIAN_POINT ( 'NONE',  ( 609.6990281814310038, 187.8427340524074225, -188.9822575857425022 ) ) ;
#5513=ORIENTED_EDGE ( 'NONE', *, *, #9087, .F. ) ;
#5562=CARTESIAN_POINT ( 'NONE',  ( 609.6829874266189790, 186.4320250235422805, -187.4339272673398398 ) ) ;
#5602=ORIENTED_EDGE ( 'NONE', *, *, #7666, .T. ) ;
#5614=DIRECTION ( 'NONE',  ( -1.000000000000000000, 0.000000000000000000, 0.000000000000000000 ) ) ;
#5617=AXIS2_PLACEMENT_3D ( 'NONE', #12629, #2510, #7016 ) ;
#5623=DIRECTION ( 'NONE',  ( -1.000000000000000000, 0.000000000000000000, 0.000000000000000000 ) ) ;
#5629=AXIS2_PLACEMENT_3D ( 'NONE', #1170, #13431, #1092 ) ;
#5630=CARTESIAN_POINT ( 'NONE',  ( -9.137956343301000928, 374.5525593289319204, -169.9999999999999716 ) ) ;
#5635=CARTESIAN_POINT ( 'NONE',  ( 609.7043258424479291, 187.8603929224640581, -188.9582675804705332 ) ) ;
#5647=AXIS2_PLACEMENT_3D ( 'NONE', #323, #700, #14228 ) ;
#5657=ORIENTED_EDGE ( 'NONE', *, *, #9348, .T. ) ;
#5690=DIRECTION ( 'NONE',  ( 0.9578262852211514300, -0.2873478855663454401, 0.000000000000000000 ) ) ;
#5725=DIRECTION ( 'NONE',  ( 0.000000000000000000, -0.000000000000000000, 1.000000000000000000 ) ) ;
#5767=UNCERTAINTY_MEASURE_WITH_UNIT (LENGTH_MEASURE( 1.000000000000000082E-05 ), #8862, 'distance_accuracy_value', 'NONE');
#5804=ORIENTED_EDGE ( 'NONE', *, *, #9135, .T. ) ;
#5861=EDGE_LOOP ( 'NONE', ( #1868, #8886, #6528, #7936 ) ) ;
#5871=FACE_OUTER_BOUND ( 'NONE', #4443, .T. ) ;
#5905=( NAMED_UNIT ( * ) PLANE_ANGLE_UNIT ( ) SI_UNIT ( $, .RADIAN. ) );
#5913=DIRECTION ( 'NONE',  ( 0.9578262852211513190, -0.2873478855663453291, 0.000000000000000000 ) ) ;
#5929=DIRECTION ( 'NONE',  ( 0.9578262852211513190, -0.2873478855663453846, -8.575812866481462478E-17 ) ) ;
#5968=CARTESIAN_POINT ( 'NONE',  ( 142.4540310085880606, 355.9707293956415697, -187.0000000000000000 ) ) ;
#5969=ORIENTED_EDGE ( 'NONE', *, *, #4207, .T. ) ;
#6018=DIRECTION ( 'NONE',  ( 0.9578262852211513190, -0.2873478855663453846, 0.000000000000000000 ) ) ;
#6025=DIRECTION ( 'NONE',  ( -1.000000000000000000, 0.000000000000000000, 0.000000000000000000 ) ) ;
#6043=DIRECTION ( 'NONE',  ( 0.000000000000000000, 0.000000000000000000, -1.000000000000000000 ) ) ;
#6060=ADVANCED_FACE ( 'NONE', ( #6955 ), #2516, .F. ) ;
#6063=ORIENTED_EDGE ( 'NONE', *, *, #3510, .F. ) ;
#6166=ORIENTED_EDGE ( 'NONE', *, *, #13021, .T. ) ;
#6170=STYLED_ITEM ( 'NONE', ( #11029 ), #8625 ) ;
#6173=EDGE_CURVE ( 'NONE', #9769, #13350, #11473, .T. ) ;
#6184=EDGE_LOOP ( 'NONE', ( #13945, #5804 ) ) ;
#6191=AXIS2_PLACEMENT_3D ( 'NONE', #3012, #14376, #11127 ) ;
#6194=CARTESIAN_POINT ( 'NONE',  ( 610.4468987511024807, 188.9818594558784355, -185.9044171606945497 ) ) ;
#6209=PLANE ( 'NONE',  #814 ) ;
#6284=ADVANCED_FACE ( 'NONE', ( #9421 ), #3895, .F. ) ;
#6296=ORIENTED_EDGE ( 'NONE', *, *, #373, .F. ) ;
#6298=EDGE_LOOP ( 'NONE', ( #14175, #3867, #1892, #5657 ) ) ;
#6317=VERTEX_POINT ( 'NONE', #388 ) ;
#6323=ORIENTED_EDGE ( 'NONE', *, *, #1046, .T. ) ;
#6329=ORIENTED_EDGE ( 'NONE', *, *, #12076, .F. ) ;
#6332=CARTESIAN_POINT ( 'NONE',  ( 610.7992194312785159, 188.5714065965581483, -184.9452975700425554 ) ) ;
#6363=CARTESIAN_POINT ( 'NONE',  ( 609.6836880993740806, 187.1145182921505921, -188.2379512264755874 ) ) ;
#6394=CARTESIAN_POINT ( 'NONE',  ( -9.999999999999998224, 376.8992337277234128, -187.0000000000000000 ) ) ;
#6398=ORIENTED_EDGE ( 'NONE', *, *, #2214, .T. ) ;
#6417=DIRECTION ( 'NONE',  ( 1.000000000000000000, 0.000000000000000000, 0.000000000000000000 ) ) ;
#6440=VERTEX_POINT ( 'NONE', #9721 ) ;
#6449=LINE ( 'NONE', #10940, #8026 ) ;
#6472=FILL_AREA_STYLE ('',( #4254 ) ) ;
#6509=FACE_OUTER_BOUND ( 'NONE', #5475, .T. ) ;
#6512=CARTESIAN_POINT ( 'NONE',  ( 609.9372209285376130, 185.6979141947072378, -185.1431837845556743 ) ) ;
#6528=ORIENTED_EDGE ( 'NONE', *, *, #13871, .T. ) ;
#6570=AXIS2_PLACEMENT_3D ( 'NONE', #2733, #7094, #5045 ) ;
#6578=DIRECTION ( 'NONE',  ( -0.9578262852211514300, 0.2873478855663453846, 9.382948195091500646E-16 ) ) ;
#6582=VECTOR ( 'NONE', #12101, 1000.000000000000114 ) ;
#6604=ORIENTED_EDGE ( 'NONE', *, *, #357, .F. ) ;
#6662=CARTESIAN_POINT ( 'NONE',  ( -9.137956343300997375, 374.5525593289318635, -169.9999999999999716 ) ) ;
#6680=EDGE_LOOP ( 'NONE', ( #6329, #10354, #11924, #11247 ) ) ;
#6681=CARTESIAN_POINT ( 'NONE',  ( 610.0000000000001137, 191.1080398579019288, -190.0300000000000296 ) ) ;
#6723=DIRECTION ( 'NONE',  ( 0.9578262852211513190, -0.2873478855663453846, -0.000000000000000000 ) ) ;
#6744=CARTESIAN_POINT ( 'NONE',  ( -9.137956343300945861, 374.5525593289318635, -184.8000000000000114 ) ) ;
#6757=CYLINDRICAL_SURFACE ( 'NONE', #13962, 2.649999999999985700 ) ;
#6764=AXIS2_PLACEMENT_3D ( 'NONE', #10493, #12709, #11600 ) ;
#6778=ORIENTED_EDGE ( 'NONE', *, *, #4148, .T. ) ;
#6784=( GEOMETRIC_REPRESENTATION_CONTEXT ( 3 ) GLOBAL_UNCERTAINTY_ASSIGNED_CONTEXT ( ( #5767 ) ) GLOBAL_UNIT_ASSIGNED_CONTEXT ( ( #8862, #5905, #345 ) ) REPRESENTATION_CONTEXT ( 'NONE', 'WORKASPACE' ) );
#6788=ORIENTED_EDGE ( 'NONE', *, *, #12216, .F. ) ;
#6797=DIRECTION ( 'NONE',  ( 0.000000000000000000, 0.000000000000000000, -1.000000000000000000 ) ) ;
#6812=CARTESIAN_POINT ( 'NONE',  ( 609.6767525226840689, 186.8636552924789669, -187.9956429438695977 ) ) ;
#6832=AXIS2_PLACEMENT_3D ( 'NONE', #14405, #6578, #13295 ) ;
#6836=AXIS2_PLACEMENT_3D ( 'NONE', #9043, #11401, #3431 ) ;
#6846=ORIENTED_EDGE ( 'NONE', *, *, #2595, .F. ) ;
#6893=CARTESIAN_POINT ( 'NONE',  ( 610.4437618601435815, 188.9679398019578116, -185.9079617568160074 ) ) ;
#6910=ORIENTED_EDGE ( 'NONE', *, *, #13871, .F. ) ;
#6955=FACE_OUTER_BOUND ( 'NONE', #9940, .T. ) ;
#6980=ORIENTED_EDGE ( 'NONE', *, *, #1273, .T. ) ;
#7016=DIRECTION ( 'NONE',  ( -1.000000000000000000, 0.000000000000000000, 0.000000000000000000 ) ) ;
#7031=CARTESIAN_POINT ( 'NONE',  ( 610.1840840298345938, 189.9120001624725376, -186.6958543268122526 ) ) ;
#7041=ORIENTED_EDGE ( 'NONE', *, *, #6173, .F. ) ;
#7088=CIRCLE ( 'NONE', #10391, 2.649999999999985700 ) ;
#7089=CARTESIAN_POINT ( 'NONE',  ( 443.6584422793565636, 264.0194060144110608, -187.0000000000000000 ) ) ;
#7094=DIRECTION ( 'NONE',  ( 0.9578262852211508749, -0.2873478855663470499, 0.000000000000000000 ) ) ;
#7109=( GEOMETRIC_REPRESENTATION_CONTEXT ( 3 ) GLOBAL_UNCERTAINTY_ASSIGNED_CONTEXT ( ( #9312 ) ) GLOBAL_UNIT_ASSIGNED_CONTEXT ( ( #5222, #8604, #13180 ) ) REPRESENTATION_CONTEXT ( 'NONE', 'WORKASPACE' ) );
#7115=CARTESIAN_POINT ( 'NONE',  ( 610.3730626637085379, 189.1846890958936740, -186.1333820183295984 ) ) ;
#7124=VERTEX_POINT ( 'NONE', #8622 ) ;
#7125=ORIENTED_EDGE ( 'NONE', *, *, #9862, .F. ) ;
#7144=DIRECTION ( 'NONE',  ( -9.028085479645851510E-15, -3.009361826548617065E-14, -1.000000000000000000 ) ) ;
#7161=CARTESIAN_POINT ( 'NONE',  ( 139.8040310085880833, 355.9707293956415697, -187.0000000000000000 ) ) ;
#7170=PLANE ( 'NONE',  #6570 ) ;
#7175=ORIENTED_EDGE ( 'NONE', *, *, #507, .F. ) ;
#7232=PRODUCT_DEFINITION_CONTEXT ( 'detailed design', #13570, 'design' ) ;
#7245=DIRECTION ( 'NONE',  ( 2.022127743178574844E-16, 3.939404418192334771E-15, -1.000000000000000000 ) ) ;
#7248=CARTESIAN_POINT ( 'NONE',  ( 610.0000000000001137, 191.1080398579018720, -190.0000000000000000 ) ) ;
#7285=VERTEX_POINT ( 'NONE', #11346 ) ;
#7299=LINE ( 'NONE', #1828, #11734 ) ;
#7324=AXIS2_PLACEMENT_3D ( 'NONE', #7523, #4139, #861 ) ;
#7348=PLANE ( 'NONE',  #3581 ) ;
#7357=FACE_OUTER_BOUND ( 'NONE', #6680, .T. ) ;
#7370=CARTESIAN_POINT ( 'NONE',  ( 610.1557962250110450, 190.0426856094898085, -186.7771368031600048 ) ) ;
#7371=LINE ( 'NONE', #9442, #4972 ) ;
#7374=PRODUCT ( 'Mirrorsliding track^MAS-180', 'Mirrorsliding track^MAS-180', '', ( #8793 ) ) ;
#7378=ADVANCED_FACE ( 'NONE', ( #9648 ), #12889, .F. ) ;
#7381=VECTOR ( 'NONE', #1057, 1000.000000000000114 ) ;
#7398=LINE ( 'NONE', #1926, #2608 ) ;
#7399=ORIENTED_EDGE ( 'NONE', *, *, #12774, .F. ) ;
#7416=ORIENTED_EDGE ( 'NONE', *, *, #11596, .T. ) ;
#7432=EDGE_CURVE ( 'NONE', #3037, #1456, #2813, .T. ) ;
#7439=VECTOR ( 'NONE', #9535, 1000.000000000000114 ) ;
#7463=CARTESIAN_POINT ( 'NONE',  ( 609.7645211877446627, 186.0291131959509698, -186.4810828243464016 ) ) ;
#7523=CARTESIAN_POINT ( 'NONE',  ( 101.4713065522755215, 338.2376885075850623, 1.342499394901007523E-12 ) ) ;
#7567=EDGE_CURVE ( 'NONE', #6440, #12655, #14149, .T. ) ;
#7610=VERTEX_POINT ( 'NONE', #2652 ) ;
#7625=CARTESIAN_POINT ( 'NONE',  ( 610.0000000000001137, 185.6790804732684705, -184.8000000000000398 ) ) ;
#7635=CYLINDRICAL_SURFACE ( 'NONE', #2548, 2.199999999999984635 ) ;
#7640=ORIENTED_EDGE ( 'NONE', *, *, #11246, .T. ) ;
#7646=ORIENTED_EDGE ( 'NONE', *, *, #10275, .T. ) ;
#7666=EDGE_CURVE ( 'NONE', #2593, #9335, #2535, .T. ) ;
#7711=DIRECTION ( 'NONE',  ( -0.2873478855663453291, -0.9578262852211513190, -3.835990623682899812E-15 ) ) ;
#7714=SURFACE_STYLE_FILL_AREA ( #6472 ) ;
#7730=STYLED_ITEM('',(#14688),#2587);
#7734=ORIENTED_EDGE ( 'NONE', *, *, #6173, .T. ) ;
#7762=DIRECTION ( 'NONE',  ( -1.000000000000000000, 0.000000000000000000, 0.000000000000000000 ) ) ;
#7769=EDGE_CURVE ( 'NONE', #4552, #10951, #678, .T. ) ;
#7791=CARTESIAN_POINT ( 'NONE',  ( -8.074769166705396017, 378.0965165842501392, -187.0000000000000284 ) ) ;
#7792=VECTOR ( 'NONE', #3124, 1000.000000000000000 ) ;
#7812=FACE_OUTER_BOUND ( 'NONE', #3773, .T. ) ;
#7857=EDGE_LOOP ( 'NONE', ( #11855, #3361, #11167, #8227 ) ) ;
#7858=CARTESIAN_POINT ( 'NONE',  ( 610.8620436566991430, 188.5525593289318920, -187.0000000000000000 ) ) ;
#7866=CARTESIAN_POINT ( 'NONE',  ( 609.8668404561643683, 185.6877074168924935, -185.4847245573741930 ) ) ;
#7880=DIRECTION ( 'NONE',  ( -0.000000000000000000, -0.000000000000000000, 1.000000000000000000 ) ) ;
#7883=LINE ( 'NONE', #11413, #8312 ) ;
#7897=VERTEX_POINT ( 'NONE', #5491 ) ;
#7936=ORIENTED_EDGE ( 'NONE', *, *, #12847, .F. ) ;
#7991=CARTESIAN_POINT ( 'NONE',  ( 610.3661002516460030, 189.1614810556852717, -186.1520027839448232 ) ) ;
#7998=EDGE_CURVE ( 'NONE', #6317, #5365, #11325, .T. ) ;
#8003=ORIENTED_EDGE ( 'NONE', *, *, #7432, .F. ) ;
#8026=VECTOR ( 'NONE', #6723, 1000.000000000000114 ) ;
#8098=LINE ( 'NONE', #12533, #13198 ) ;
#8102=ORIENTED_EDGE ( 'NONE', *, *, #3203, .T. ) ;
#8156=VERTEX_POINT ( 'NONE', #9760 ) ;
#8157=EDGE_CURVE ( 'NONE', #12715, #2075, #7398, .T. ) ;
#8221=EDGE_CURVE ( 'NONE', #10951, #1218, #2962, .T. ) ;
#8227=ORIENTED_EDGE ( 'NONE', *, *, #1576, .T. ) ;
#8289=CARTESIAN_POINT ( 'NONE',  ( 610.6294623944595514, 188.6821150189054777, -185.3758453455904771 ) ) ;
#8312=VECTOR ( 'NONE', #10301, 1000.000000000000000 ) ;
#8339=ADVANCED_FACE ( 'NONE', ( #4589 ), #12460, .F. ) ;
#8364=ORIENTED_EDGE ( 'NONE', *, *, #3902, .T. ) ;
#8391=CARTESIAN_POINT ( 'NONE',  ( 610.8620436566991430, 188.5525593289319488, -184.8000000000000398 ) ) ;
#8394=ORIENTED_EDGE ( 'NONE', *, *, #9171, .T. ) ;
#8435=CIRCLE ( 'NONE', #10326, 2.649999999999985700 ) ;
#8446=EDGE_CURVE ( 'NONE', #8156, #6317, #12616, .T. ) ;
#8464=ORIENTED_EDGE ( 'NONE', *, *, #12216, .T. ) ;
#8477=ORIENTED_EDGE ( 'NONE', *, *, #1214, .T. ) ;
#8498=VECTOR ( 'NONE', #3937, 1000.000000000000000 ) ;
#8503=CARTESIAN_POINT ( 'NONE',  ( 609.8294541519869654, 189.4056243435263980, -189.7329333695814739 ) ) ;
#8514=CARTESIAN_POINT ( 'NONE',  ( 142.4540310085880606, 355.9707293956415697, -190.0000000000000000 ) ) ;
#8524=( GEOMETRIC_REPRESENTATION_CONTEXT ( 3 ) GLOBAL_UNCERTAINTY_ASSIGNED_CONTEXT ( ( #12696 ) ) GLOBAL_UNIT_ASSIGNED_CONTEXT ( ( #9936, #1962, #10820 ) ) REPRESENTATION_CONTEXT ( 'NONE', 'WORKASPACE' ) );
#8534=CARTESIAN_POINT ( 'NONE',  ( 446.3084422793565409, 264.0194060144110608, -187.0000000000000000 ) ) ;
#8604=( NAMED_UNIT ( * ) PLANE_ANGLE_UNIT ( ) SI_UNIT ( $, .RADIAN. ) );
#8622=CARTESIAN_POINT ( 'NONE',  ( -10.00000000000004263, 371.6790804732683569, -169.9999999999999716 ) ) ;
#8625=ADVANCED_BREP_SHAPE_REPRESENTATION ( '', ( #2587, #9440 ), #8524 ) ;
#8642=PRODUCT_DEFINITION ( 'UNKNOWN', '', #5255, #7232 ) ;
#8646=CARTESIAN_POINT ( 'NONE',  ( 609.6939753585367043, 187.4861613156657540, -188.5968284039610978 ) ) ;
#8648=DIRECTION ( 'NONE',  ( 0.000000000000000000, 0.000000000000000000, -1.000000000000000000 ) ) ;
#8653=VECTOR ( 'NONE', #1301, 1000.000000000000000 ) ;
#8663=DIRECTION ( 'NONE',  ( 0.000000000000000000, 0.000000000000000000, -1.000000000000000000 ) ) ;
#8677=PLANE ( 'NONE',  #8926 ) ;
#8736=FACE_OUTER_BOUND ( 'NONE', #12215, .T. ) ;
#8750=ADVANCED_FACE ( 'NONE', ( #4555, #4700, #13549 ), #13770, .F. ) ;
#8762=COLOUR_RGB ( '',0.8941176470588234615, 0.8941176470588234615, 0.8941176470588234615 ) ;
#8793=PRODUCT_CONTEXT ( 'NONE', #9611, 'mechanical' ) ;
#8798=CARTESIAN_POINT ( 'NONE',  ( 446.3084422793565409, 264.0194060144110608, -187.0000000000000000 ) ) ;
#8862=( LENGTH_UNIT ( ) NAMED_UNIT ( * ) SI_UNIT ( .MILLI., .METRE. ) );
#8871=CARTESIAN_POINT ( 'NONE',  ( 448.9584422793565750, 264.0194060144110608, -190.0000000000000000 ) ) ;
#8886=ORIENTED_EDGE ( 'NONE', *, *, #3902, .F. ) ;
#8916=VECTOR ( 'NONE', #13763, 1000.000000000000114 ) ;
#8925=VECTOR ( 'NONE', #5929, 1000.000000000000114 ) ;
#8926=AXIS2_PLACEMENT_3D ( 'NONE', #2997, #13182, #1967 ) ;
#8936=CYLINDRICAL_SURFACE ( 'NONE', #676, 2.649999999999985700 ) ;
#8957=EDGE_LOOP ( 'NONE', ( #7646, #8464, #1678, #10892, #6604, #13465, #8364 ) ) ;
#9006=CARTESIAN_POINT ( 'NONE',  ( 610.0000000000001137, 185.6790804732684705, -184.8000000000000398 ) ) ;
#9030=LINE ( 'NONE', #12483, #662 ) ;
#9036=CARTESIAN_POINT ( 'NONE',  ( 609.8556724072889210, 189.7221213180926611, -189.8938770989753095 ) ) ;
#9043=CARTESIAN_POINT ( 'NONE',  ( 446.3084422793565409, 264.0194060144110608, -190.0000000000000000 ) ) ;
#9087=EDGE_CURVE ( 'NONE', #3684, #9769, #2985, .T. ) ;
#9102=CARTESIAN_POINT ( 'NONE',  ( 610.0000000000001137, 191.1080398579019572, -187.0000000000000284 ) ) ;
#9118=ORIENTED_EDGE ( 'NONE', *, *, #583, .F. ) ;
#9135=EDGE_CURVE ( 'NONE', #11808, #10071, #3342, .T. ) ;
#9140=ORIENTED_EDGE ( 'NONE', *, *, #14587, .F. ) ;
#9171=EDGE_CURVE ( 'NONE', #9848, #12715, #13460, .T. ) ;
#9178=CARTESIAN_POINT ( 'NONE',  ( 609.7455576527837593, 188.4502455723027481, -189.3436892194421546 ) ) ;
#9184=ORIENTED_EDGE ( 'NONE', *, *, #11596, .F. ) ;
#9286=ORIENTED_EDGE ( 'NONE', *, *, #9945, .T. ) ;
#9305=CARTESIAN_POINT ( 'NONE',  ( -9.999999999999957367, 376.8992337277236970, -187.0000000000000000 ) ) ;
#9312=UNCERTAINTY_MEASURE_WITH_UNIT (LENGTH_MEASURE( 1.000000000000000082E-05 ), #5222, 'distance_accuracy_value', 'NONE');
#9335=VERTEX_POINT ( 'NONE', #4976 ) ;
#9348=EDGE_CURVE ( 'NONE', #12661, #2075, #5112, .T. ) ;
#9402=CARTESIAN_POINT ( 'NONE',  ( -10.00000000000000000, 413.4403065089105667, -190.0000000000000000 ) ) ;
#9408=CIRCLE ( 'NONE', #5629, 2.649999999999985700 ) ;
#9421=FACE_OUTER_BOUND ( 'NONE', #10885, .T. ) ;
#9430=CARTESIAN_POINT ( 'NONE',  ( 610.0000000000000000, 227.4403065089105951, -187.0000000000000000 ) ) ;
#9440=AXIS2_PLACEMENT_3D ( 'NONE', #4347, #14302, #6417 ) ;
#9441=CARTESIAN_POINT ( 'NONE',  ( 610.4899793196105975, 188.8968529749589038, -185.7755421771552165 ) ) ;
#9442=CARTESIAN_POINT ( 'NONE',  ( 610.8620436566991430, 188.5525593289318920, -184.8000000000000682 ) ) ;
#9498=ADVANCED_FACE ( 'NONE', ( #2060 ), #811, .F. ) ;
#9535=DIRECTION ( 'NONE',  ( 0.9578262852211513190, -0.2873478855663453846, -0.000000000000000000 ) ) ;
#9552=FACE_BOUND ( 'NONE', #6184, .T. ) ;
#9584=CARTESIAN_POINT ( 'NONE',  ( 610.7405786874708156, 188.6041887390371130, -185.0905558487023370 ) ) ;
#9588=DIRECTION ( 'NONE',  ( -8.745957808406929547E-15, -2.915319269468972624E-14, -1.000000000000000000 ) ) ;
#9611=APPLICATION_CONTEXT ( 'automotive_design' ) ;
#9623=CARTESIAN_POINT ( 'NONE',  ( -8.505790995055050985, 376.6597771564184995, -184.8000000000000398 ) ) ;
#9648=FACE_OUTER_BOUND ( 'NONE', #2308, .T. ) ;
#9681=CARTESIAN_POINT ( 'NONE',  ( -112.9080459801079144, 33.87241379403258890, -190.0000000000000000 ) ) ;
#9703=ORIENTED_EDGE ( 'NONE', *, *, #9945, .F. ) ;
#9709=VECTOR ( 'NONE', #8663, 1000.000000000000000 ) ;
#9721=CARTESIAN_POINT ( 'NONE',  ( 443.6584422793565636, 264.0194060144110608, -190.0000000000000000 ) ) ;
#9760=CARTESIAN_POINT ( 'NONE',  ( 137.1540310085880776, 355.9707293956415697, -190.0000000000000000 ) ) ;
#9767=CARTESIAN_POINT ( 'NONE',  ( 609.7206935199311602, 188.0285076711449790, -189.0295014234984023 ) ) ;
#9769=VERTEX_POINT ( 'NONE', #3633 ) ;
#9786=DIRECTION ( 'NONE',  ( 0.000000000000000000, 0.000000000000000000, -1.000000000000000000 ) ) ;
#9840=ORIENTED_EDGE ( 'NONE', *, *, #7567, .F. ) ;
#9848=VERTEX_POINT ( 'NONE', #4303 ) ;
#9862=EDGE_CURVE ( 'NONE', #3037, #3179, #14412, .T. ) ;
#9912=CARTESIAN_POINT ( 'NONE',  ( -8.505790995054926640, 376.6597771564183859, -187.0000000000000000 ) ) ;
#9919=ORIENTED_EDGE ( 'NONE', *, *, #12774, .T. ) ;
#9921=CARTESIAN_POINT ( 'NONE',  ( 446.3084422793565409, 264.0194060144110608, -187.0000000000000000 ) ) ;
#9936=( LENGTH_UNIT ( ) NAMED_UNIT ( * ) SI_UNIT ( .MILLI., .METRE. ) );
#9940=EDGE_LOOP ( 'NONE', ( #13056, #13915, #10681, #8102 ) ) ;
#9942=EDGE_CURVE ( 'NONE', #1456, #7897, #6449, .T. ) ;
#9945=EDGE_CURVE ( 'NONE', #12403, #8156, #7088, .T. ) ;
#9962=VECTOR ( 'NONE', #2930, 1000.000000000000000 ) ;
#9991=CARTESIAN_POINT ( 'NONE',  ( 610.0000000000000000, 227.4403065089105951, -187.0000000000000000 ) ) ;
#10061=CARTESIAN_POINT ( 'NONE',  ( 609.7814593570623174, 185.8554382275811463, -186.1689414351991161 ) ) ;
#10071=VERTEX_POINT ( 'NONE', #7089 ) ;
#10097=CIRCLE ( 'NONE', #11977, 5.199999999999999289 ) ;
#10192=DIRECTION ( 'NONE',  ( 0.2873478855663453846, 0.9578262852211513190, 0.000000000000000000 ) ) ;
#10218=CARTESIAN_POINT ( 'NONE',  ( 610.1796992002056186, 189.8973840637093247, -186.7223300543793698 ) ) ;
#10248=CARTESIAN_POINT ( 'NONE',  ( 610.0832774997078332, 190.4835367118463125, -186.9433982284626552 ) ) ;
#10275=EDGE_CURVE ( 'NONE', #7285, #13752, #11058, .T. ) ;
#10301=DIRECTION ( 'NONE',  ( -0.000000000000000000, -0.000000000000000000, 1.000000000000000000 ) ) ;
#10326=AXIS2_PLACEMENT_3D ( 'NONE', #7161, #6043, #198 ) ;
#10354=ORIENTED_EDGE ( 'NONE', *, *, #10275, .F. ) ;
#10391=AXIS2_PLACEMENT_3D ( 'NONE', #11000, #8648, #5614 ) ;
#10427=ORIENTED_EDGE ( 'NONE', *, *, #7998, .F. ) ;
#10459=DIRECTION ( 'NONE',  ( 1.000000000000000000, 0.000000000000000000, -0.000000000000000000 ) ) ;
#10473=DIRECTION ( 'NONE',  ( -0.9578262852211513190, 0.2873478855663453846, 8.575812866481462478E-17 ) ) ;
#10493=CARTESIAN_POINT ( 'NONE',  ( 610.0000000000001137, 185.6790804732683853, -169.9999999999999716 ) ) ;
#10496=CARTESIAN_POINT ( 'NONE',  ( 610.0000000000001137, 185.6790804732684137, -184.8000000000000682 ) ) ;
#10518=CARTESIAN_POINT ( 'NONE',  ( 610.0000000000000000, 227.4403065089105951, -187.0000000000000000 ) ) ;
#10521=CARTESIAN_POINT ( 'NONE',  ( -10.00000000000000000, 371.6790804732683569, -187.0000000000000000 ) ) ;
#10523=ORIENTED_EDGE ( 'NONE', *, *, #4148, .F. ) ;
#10526=PLANE ( 'NONE',  #13402 ) ;
#10627=AXIS2_PLACEMENT_3D ( 'NONE', #11304, #1110, #5623 ) ;
#10630=ORIENTED_EDGE ( 'NONE', *, *, #11246, .F. ) ;
#10638=LINE ( 'NONE', #11513, #7439 ) ;
#10658=CARTESIAN_POINT ( 'NONE',  ( 610.0858458365329398, 190.4893660822393144, -186.9132285165672727 ) ) ;
#10681=ORIENTED_EDGE ( 'NONE', *, *, #3872, .T. ) ;
#10685=ORIENTED_EDGE ( 'NONE', *, *, #9087, .T. ) ;
#10708=CARTESIAN_POINT ( 'NONE',  ( -10.00000000000003730, 371.6790804732684137, -169.9999999999999716 ) ) ;
#10720=CARTESIAN_POINT ( 'NONE',  ( 609.6990795428844194, 187.6157354204721912, -188.7107384553189888 ) ) ;
#10729=LINE ( 'NONE', #3880, #10807 ) ;
#10735=EDGE_LOOP ( 'NONE', ( #6778, #7041, #5513, #5969 ) ) ;
#10740=ORIENTED_EDGE ( 'NONE', *, *, #8446, .F. ) ;
#10767=AXIS2_PLACEMENT_3D ( 'NONE', #10521, #10459, #319 ) ;
#10807=VECTOR ( 'NONE', #368, 1000.000000000000000 ) ;
#10820=( NAMED_UNIT ( * ) SI_UNIT ( $, .STERADIAN. ) SOLID_ANGLE_UNIT ( ) );
#10834=AXIS2_PLACEMENT_3D ( 'NONE', #8534, #13935, #6025 ) ;
#10847=DIRECTION ( 'NONE',  ( 0.9578262852211513190, -0.2873478855663454401, -2.126837879698859960E-31 ) ) ;
#10849=DIRECTION ( 'NONE',  ( 0.2873478855663471054, 0.9578262852211508749, -1.632680918566126195E-14 ) ) ;
#10885=EDGE_LOOP ( 'NONE', ( #6910, #5602, #4227, #10630 ) ) ;
#10892=ORIENTED_EDGE ( 'NONE', *, *, #4207, .F. ) ;
#10929=DIRECTION ( 'NONE',  ( 0.2873478855663453291, 0.9578262852211513190, 0.000000000000000000 ) ) ;
#10940=CARTESIAN_POINT ( 'NONE',  ( -8.505790995055066972, 376.6597771564184427, -187.0000000000000284 ) ) ;
#10948=ADVANCED_FACE ( 'NONE', ( #5871 ), #6757, .F. ) ;
#10951=VERTEX_POINT ( 'NONE', #11552 ) ;
#10985=PLANE ( 'NONE',  #7324 ) ;
#11000=CARTESIAN_POINT ( 'NONE',  ( 139.8040310085880833, 355.9707293956415697, -190.0000000000000000 ) ) ;
#11022=ADVANCED_FACE ( 'NONE', ( #12738 ), #7348, .F. ) ;
#11029=PRESENTATION_STYLE_ASSIGNMENT (( #694 ) ) ;
#11058=LINE ( 'NONE', #3176, #11334 ) ;
#11127=DIRECTION ( 'NONE',  ( -0.2873478855663437748, -0.9578262852211518741, -0.000000000000000000 ) ) ;
#11167=ORIENTED_EDGE ( 'NONE', *, *, #3339, .F. ) ;
#11217=EDGE_LOOP ( 'NONE', ( #3325, #1357, #3748, #6063 ) ) ;
#11218=CYLINDRICAL_SURFACE ( 'NONE', #11263, 2.649999999999985700 ) ;
#11225=DIRECTION ( 'NONE',  ( -1.000000000000000000, 0.000000000000000000, 0.000000000000000000 ) ) ;
#11241=CARTESIAN_POINT ( 'NONE',  ( 609.6698590453944462, 186.8406770348469195, -188.0140793454688151 ) ) ;
#11246=EDGE_CURVE ( 'NONE', #7610, #1236, #14500, .T. ) ;
#11247=ORIENTED_EDGE ( 'NONE', *, *, #8221, .F. ) ;
#11254=ADVANCED_FACE ( 'NONE', ( #3362 ), #1213, .T. ) ;
#11263=AXIS2_PLACEMENT_3D ( 'NONE', #8798, #12106, #13520 ) ;
#11287=SHAPE_DEFINITION_REPRESENTATION ( #962, #342 ) ;
#11304=CARTESIAN_POINT ( 'NONE',  ( 139.8040310085880833, 355.9707293956415697, -187.0000000000000000 ) ) ;
#11313=VECTOR ( 'NONE', #540, 1000.000000000000000 ) ;
#11321=CARTESIAN_POINT ( 'NONE',  ( -9.511508594537115613, 378.5275384125997107, -190.0000000000000000 ) ) ;
#11323=LINE ( 'NONE', #7791, #7381 ) ;
#11325=CIRCLE ( 'NONE', #10627, 2.649999999999985700 ) ;
#11334=VECTOR ( 'NONE', #5318, 1000.000000000000114 ) ;
#11346=CARTESIAN_POINT ( 'NONE',  ( -9.511508594537115613, 378.5275384125997107, -187.0000000000000000 ) ) ;
#11349=AXIS2_PLACEMENT_3D ( 'NONE', #9921, #13376, #14427 ) ;
#11357=VECTOR ( 'NONE', #2234, 1000.000000000000000 ) ;
#11362=DIRECTION ( 'NONE',  ( -0.000000000000000000, -0.000000000000000000, 1.000000000000000000 ) ) ;
#11401=DIRECTION ( 'NONE',  ( 0.000000000000000000, 0.000000000000000000, -1.000000000000000000 ) ) ;
#11413=CARTESIAN_POINT ( 'NONE',  ( 443.6584422793565636, 264.0194060144110608, -187.0000000000000000 ) ) ;
#11473=LINE ( 'NONE', #1368, #8653 ) ;
#11480=AXIS2_PLACEMENT_3D ( 'NONE', #2507, #6797, #11225 ) ;
#11513=CARTESIAN_POINT ( 'NONE',  ( -8.505790995055079406, 376.6597771564183859, -190.0000000000000284 ) ) ;
#11533=CARTESIAN_POINT ( 'NONE',  ( 610.2394425817745969, 189.6441153868865399, -186.5350371479513569 ) ) ;
#11552=CARTESIAN_POINT ( 'NONE',  ( -8.074769166705394241, 378.0965165842501392, -190.0000000000000000 ) ) ;
#11560=EDGE_LOOP ( 'NONE', ( #9840, #4041 ) ) ;
#11596=EDGE_CURVE ( 'NONE', #7897, #12715, #404, .T. ) ;
#11600=DIRECTION ( 'NONE',  ( 0.000000000000000000, -1.000000000000000000, -3.344232600703091053E-15 ) ) ;
#11636=CARTESIAN_POINT ( 'NONE',  ( 610.0000000000000000, 227.4403065089105951, -187.0000000000000000 ) ) ;
#11680=CARTESIAN_POINT ( 'NONE',  ( -10.00000000000000000, 371.6790804732683569, -187.0000000000000000 ) ) ;
#11734=VECTOR ( 'NONE', #10847, 1000.000000000000227 ) ;
#11775=ADVANCED_FACE ( 'NONE', ( #7812 ), #3227, .T. ) ;
#11785=CARTESIAN_POINT ( 'NONE',  ( 610.2366331756301179, 189.6374102278066971, -186.5502271136477361 ) ) ;
#11807=FACE_OUTER_BOUND ( 'NONE', #762, .T. ) ;
#11808=VERTEX_POINT ( 'NONE', #5241 ) ;
#11855=ORIENTED_EDGE ( 'NONE', *, *, #583, .T. ) ;
#11863=CARTESIAN_POINT ( 'NONE',  ( 610.1812141201095301, 189.9029010627875493, -186.7093446292720387 ) ) ;
#11873=CARTESIAN_POINT ( 'NONE',  ( 102.3333502089745650, 341.1111673632485122, 1.352973838917536986E-12 ) ) ;
#11875=EDGE_CURVE ( 'NONE', #6440, #10071, #7883, .T. ) ;
#11880=EDGE_CURVE ( 'NONE', #7285, #1218, #1233, .T. ) ;
#11890=CARTESIAN_POINT ( 'NONE',  ( 609.7124105659718225, 187.8865375995820557, -188.9268648956065419 ) ) ;
#11895=CARTESIAN_POINT ( 'NONE',  ( -10.00000000000000000, 413.4403065089105667, -187.0000000000000000 ) ) ;
#11924=ORIENTED_EDGE ( 'NONE', *, *, #11880, .T. ) ;
#11932=CARTESIAN_POINT ( 'NONE',  ( -9.999999999999998224, 376.8992337277234128, -187.0000000000000000 ) ) ;
#11970=CARTESIAN_POINT ( 'NONE',  ( -111.4713065522750952, 33.44139196568231398, -190.0000000000000000 ) ) ;
#11977=AXIS2_PLACEMENT_3D ( 'NONE', #1410, #2509, #12562 ) ;
#11982=ORIENTED_EDGE ( 'NONE', *, *, #1273, .F. ) ;
#12034=DIRECTION ( 'NONE',  ( -2.449021377849607626E-15, -3.265361837132810036E-15, 1.000000000000000000 ) ) ;
#12076=EDGE_CURVE ( 'NONE', #13752, #10951, #14361, .T. ) ;
#12101=DIRECTION ( 'NONE',  ( -0.2873478855663470499, -0.9578262852211508749, -0.000000000000000000 ) ) ;
#12106=DIRECTION ( 'NONE',  ( -0.000000000000000000, -0.000000000000000000, 1.000000000000000000 ) ) ;
#12215=EDGE_LOOP ( 'NONE', ( #12422, #8003, #9140, #9184 ) ) ;
#12216=EDGE_CURVE ( 'NONE', #13752, #1456, #11323, .T. ) ;
#12222=ORIENTED_EDGE ( 'NONE', *, *, #3492, .F. ) ;
#12273=CARTESIAN_POINT ( 'NONE',  ( -10.00000000000000000, 371.6790804732683569, -190.0000000000000000 ) ) ;
#12315=LINE ( 'NONE', #3399, #12439 ) ;
#12388=CARTESIAN_POINT ( 'NONE',  ( -8.505790995054899994, 376.6597771564184427, -184.8000000000000398 ) ) ;
#12401=ADVANCED_FACE ( 'NONE', ( #8736 ), #7635, .F. ) ;
#12403=VERTEX_POINT ( 'NONE', #8514 ) ;
#12418=CARTESIAN_POINT ( 'NONE',  ( -10.00000000000000888, 371.6790804732683569, -169.9999999999999716 ) ) ;
#12422=ORIENTED_EDGE ( 'NONE', *, *, #9942, .F. ) ;
#12439=VECTOR ( 'NONE', #11362, 1000.000000000000000 ) ;
#12460=PLANE ( 'NONE',  #3314 ) ;
#12483=CARTESIAN_POINT ( 'NONE',  ( 610.0000000000001137, 185.6790804732683853, -169.9999999999999716 ) ) ;
#12489=AXIS2_PLACEMENT_3D ( 'NONE', #13702, #3600, #2318 ) ;
#12493=CARTESIAN_POINT ( 'NONE',  ( 610.0000000000001137, 185.6790804732684990, -184.8000000000000966 ) ) ;
#12533=CARTESIAN_POINT ( 'NONE',  ( 610.0000000000002274, 191.1080398579018720, -187.0000000000000284 ) ) ;
#12562=DIRECTION ( 'NONE',  ( -0.2873478855663446629, -0.9578262852211516520, 0.000000000000000000 ) ) ;
#12593=DIRECTION ( 'NONE',  ( 0.000000000000000000, 0.000000000000000000, -1.000000000000000000 ) ) ;
#12616=LINE ( 'NONE', #419, #3574 ) ;
#12629=CARTESIAN_POINT ( 'NONE',  ( 139.8040310085880833, 355.9707293956415697, -190.0000000000000000 ) ) ;
#12655=VERTEX_POINT ( 'NONE', #8871 ) ;
#12661=VERTEX_POINT ( 'NONE', #5490 ) ;
#12685=DIRECTION ( 'NONE',  ( -0.000000000000000000, -0.000000000000000000, 1.000000000000000000 ) ) ;
#12696=UNCERTAINTY_MEASURE_WITH_UNIT (LENGTH_MEASURE( 1.000000000000000082E-05 ), #9936, 'distance_accuracy_value', 'NONE');
#12709=DIRECTION ( 'NONE',  ( 1.003269780210927276E-15, 3.344232600703091053E-15, -1.000000000000000000 ) ) ;
#12715=VERTEX_POINT ( 'NONE', #2673 ) ;
#12732=VECTOR ( 'NONE', #9786, 1000.000000000000000 ) ;
#12738=FACE_OUTER_BOUND ( 'NONE', #4055, .T. ) ;
#12754=LINE ( 'NONE', #11636, #5425 ) ;
#12774=EDGE_CURVE ( 'NONE', #8156, #12403, #1839, .T. ) ;
#12799=CARTESIAN_POINT ( 'NONE',  ( 610.0000000000001137, 191.1080398579019572, -186.9697000000000173 ) ) ;
#12847=EDGE_CURVE ( 'NONE', #1218, #7610, #3112, .T. ) ;
#12883=DIRECTION ( 'NONE',  ( -0.2873478855663454401, -0.9578262852211514300, 0.000000000000000000 ) ) ;
#12889=CYLINDRICAL_SURFACE ( 'NONE', #10834, 2.649999999999985700 ) ;
#12916=FACE_OUTER_BOUND ( 'NONE', #11217, .T. ) ;
#12921=VECTOR ( 'NONE', #7711, 1000.000000000000227 ) ;
#12931=LINE ( 'NONE', #2906, #13658 ) ;
#12981=CARTESIAN_POINT ( 'NONE',  ( 610.6325945170714249, 188.6953700521320911, -185.3721572044278787 ) ) ;
#13021=EDGE_CURVE ( 'NONE', #12655, #6440, #9408, .T. ) ;
#13045=SURFACE_SIDE_STYLE ('',( #7714 ) ) ;
#13056=ORIENTED_EDGE ( 'NONE', *, *, #2748, .F. ) ;
#13085=CARTESIAN_POINT ( 'NONE',  ( 609.7735223591643035, 188.7684563956151464, -189.4730470240896807 ) ) ;
#13150=VECTOR ( 'NONE', #2219, 1000.000000000000114 ) ;
#13180=( NAMED_UNIT ( * ) SI_UNIT ( $, .STERADIAN. ) SOLID_ANGLE_UNIT ( ) );
#13182=DIRECTION ( 'NONE',  ( -0.2873478855663534892, -0.9578262852211489875, 0.000000000000000000 ) ) ;
#13196=ADVANCED_FACE ( 'NONE', ( #7357 ), #8677, .T. ) ;
#13198=VECTOR ( 'NONE', #7144, 1000.000000000000000 ) ;
#13227=CARTESIAN_POINT ( 'NONE',  ( 609.6994022290995190, 186.4862707338506311, -187.4054488658613593 ) ) ;
#13229=AXIS2_PLACEMENT_3D ( 'NONE', #4782, #5725, #3434 ) ;
#13236=EDGE_LOOP ( 'NONE', ( #7399, #9703 ) ) ;
#13295=DIRECTION ( 'NONE',  ( -0.2873478855663453291, -0.9578262852211513190, -0.000000000000000000 ) ) ;
#13350=VERTEX_POINT ( 'NONE', #7248 ) ;
#13376=DIRECTION ( 'NONE',  ( 0.000000000000000000, 0.000000000000000000, -1.000000000000000000 ) ) ;
#13402=AXIS2_PLACEMENT_3D ( 'NONE', #9430, #400, #5421 ) ;
#13405=CARTESIAN_POINT ( 'NONE',  ( 139.8040310085880833, 355.9707293956415697, -187.0000000000000000 ) ) ;
#13414=VECTOR ( 'NONE', #10849, 1000.000000000000000 ) ;
#13431=DIRECTION ( 'NONE',  ( 0.000000000000000000, 0.000000000000000000, -1.000000000000000000 ) ) ;
#13441=CARTESIAN_POINT ( 'NONE',  ( 139.8040310085880833, 355.9707293956415697, -187.0000000000000000 ) ) ;
#13460=LINE ( 'NONE', #7858, #731 ) ;
#13465=ORIENTED_EDGE ( 'NONE', *, *, #7666, .F. ) ;
#13520=DIRECTION ( 'NONE',  ( -1.000000000000000000, 0.000000000000000000, 0.000000000000000000 ) ) ;
#13540=CARTESIAN_POINT ( 'NONE',  ( 609.7898554267394502, 185.8834251265051307, -186.1610889986683048 ) ) ;
#13549=FACE_OUTER_BOUND ( 'NONE', #4297, .T. ) ;
#13551=CARTESIAN_POINT ( 'NONE',  ( -8.505790995054940851, 376.6597771564182722, -190.0000000000000284 ) ) ;
#13570=APPLICATION_CONTEXT ( 'automotive_design' ) ;
#13658=VECTOR ( 'NONE', #12034, 1000.000000000000000 ) ;
#13663=LINE ( 'NONE', #3346, #13150 ) ;
#13685=CARTESIAN_POINT ( 'NONE',  ( 610.0417734222098716, 190.7948035559919333, -187.0000000000000284 ) ) ;
#13702=CARTESIAN_POINT ( 'NONE',  ( -8.505790995055050985, 376.6597771564184995, -184.8000000000000398 ) ) ;
#13752=VERTEX_POINT ( 'NONE', #3956 ) ;
#13758=CLOSED_SHELL ( 'NONE', ( #7378, #3585, #3129, #6284, #87, #8750, #11022, #1782, #13196, #11775, #11254, #8339, #4533, #12401, #590, #9498, #5061, #2729, #6060, #10948, #2584 ) ) ;
#13761=CARTESIAN_POINT ( 'NONE',  ( 610.8620436566991430, 188.5525593289319488, -184.8000000000000682 ) ) ;
#13763=DIRECTION ( 'NONE',  ( 0.2873478855663452736, 0.9578262852211513190, 3.491481338843133355E-15 ) ) ;
#13770=PLANE ( 'NONE',  #13229 ) ;
#13824=CARTESIAN_POINT ( 'NONE',  ( 610.7462142612635034, 188.6189422762846561, -185.0840554379255707 ) ) ;
#13871=EDGE_CURVE ( 'NONE', #2593, #7610, #4173, .T. ) ;
#13904=CARTESIAN_POINT ( 'NONE',  ( 610.4513696044788276, 188.9932989497419555, -185.8927021017107677 ) ) ;
#13915=ORIENTED_EDGE ( 'NONE', *, *, #1214, .F. ) ;
#13935=DIRECTION ( 'NONE',  ( -0.000000000000000000, -0.000000000000000000, 1.000000000000000000 ) ) ;
#13945=ORIENTED_EDGE ( 'NONE', *, *, #373, .T. ) ;
#13962=AXIS2_PLACEMENT_3D ( 'NONE', #13405, #7880, #2545 ) ;
#14030=DIRECTION ( 'NONE',  ( -0.9578262852211513190, 0.2873478855663453846, 0.000000000000000000 ) ) ;
#14031=LINE ( 'NONE', #14178, #1866 ) ;
#14052=PLANE ( 'NONE',  #3383 ) ;
#14054=LINE ( 'NONE', #11895, #8498 ) ;
#14096=LINE ( 'NONE', #11932, #13414 ) ;
#14112=CARTESIAN_POINT ( 'NONE',  ( 610.0000000000001137, 191.1080398579018720, -190.0000000000000000 ) ) ;
#14149=CIRCLE ( 'NONE', #6836, 2.649999999999985700 ) ;
#14159=VECTOR ( 'NONE', #14324, 1000.000000000000114 ) ;
#14168=CARTESIAN_POINT ( 'NONE',  ( 610.2669374424701800, 189.5106555248625284, -186.4579326193729969 ) ) ;
#14175=ORIENTED_EDGE ( 'NONE', *, *, #8157, .F. ) ;
#14178=CARTESIAN_POINT ( 'NONE',  ( 101.4713065522757063, 338.2376885075856876, -169.9999999999999716 ) ) ;
#14228=DIRECTION ( 'NONE',  ( -0.2873478855663452736, -0.9578262852211514300, 0.000000000000000000 ) ) ;
#14264=CARTESIAN_POINT ( 'NONE',  ( 609.7983275391768530, 185.9141716657875349, -186.1519484124941641 ) ) ;
#14273=DIRECTION ( 'NONE',  ( -0.9578262852211514300, 0.2873478855663454401, 0.000000000000000000 ) ) ;
#14289=ORIENTED_EDGE ( 'NONE', *, *, #7432, .T. ) ;
#14302=DIRECTION ( 'NONE',  ( 0.000000000000000000, 0.000000000000000000, 1.000000000000000000 ) ) ;
#14324=DIRECTION ( 'NONE',  ( -0.9578262852211489875, 0.2873478855663534892, 0.000000000000000000 ) ) ;
#14325=EDGE_CURVE ( 'NONE', #9335, #1236, #14054, .T. ) ;
#14361=LINE ( 'NONE', #5354, #9962 ) ;
#14376=DIRECTION ( 'NONE',  ( -0.9578262852211518741, 0.2873478855663437748, 0.000000000000000000 ) ) ;
#14383=EDGE_LOOP ( 'NONE', ( #2486, #14461 ) ) ;
#14405=CARTESIAN_POINT ( 'NONE',  ( 610.0000000000001137, 185.6790804732684421, -187.0000000000000000 ) ) ;
#14412=LINE ( 'NONE', #6662, #7792 ) ;
#14427=DIRECTION ( 'NONE',  ( -1.000000000000000000, 0.000000000000000000, 0.000000000000000000 ) ) ;
#14461=ORIENTED_EDGE ( 'NONE', *, *, #2595, .T. ) ;
#14500=LINE ( 'NONE', #12273, #11357 ) ;
#14568=CARTESIAN_POINT ( 'NONE',  ( 609.9913795634330427, 185.6503456847118514, -184.8000000000000966 ) ) ;
#14587=EDGE_CURVE ( 'NONE', #12715, #3037, #7371, .T. ) ;
#14682=COLOUR_RGB('Off White',0.89,0.88,0.83);
#14683=FILL_AREA_STYLE_COLOUR('',#14682);
#14684=FILL_AREA_STYLE('',(#14683));
#14685=SURFACE_STYLE_FILL_AREA(#14684);
#14686=SURFACE_SIDE_STYLE('',(#14685));
#14687=SURFACE_STYLE_USAGE(.BOTH.,#14686);
#14688=PRESENTATION_STYLE_ASSIGNMENT((#14687));
ENDSEC;
END-ISO-10303-21;
